ISO-10303-21;
HEADER;
/* Generated by software containing ST-Developer
 * from STEP Tools, Inc. (www.steptools.com) 
 */

FILE_DESCRIPTION(
/* description */ ('Fatigue rig crank-slider'),
/* implementation_level */ '2;1');

FILE_NAME(
/* name */ 'Cap Screw - M4x16.step',
/* time_stamp */ '2026-10-28T03:24:50-07:00',
/* author */ (''),
/* organization */ (''),
/* preprocessor_version */ 'ST-DEVELOPER v20.2',
/* originating_system */ 'Autodesk Translation Framework v15.17.0.0',
/* authorisation */ '');

FILE_SCHEMA (('AUTOMOTIVE_DESIGN { 1 0 10303 214 3 1 1 }'));
ENDSEC;

DATA;
#10=MECHANICAL_DESIGN_GEOMETRIC_PRESENTATION_REPRESENTATION('',(#603),#16911);
#16=CONICAL_SURFACE('',#9876,0.325,0.785398163397448);
#17=CONICAL_SURFACE('',#9880,0.335,0.785398163397448);
#18=CONICAL_SURFACE('',#9884,0.21,0.463647609000806);
#19=CONICAL_SURFACE('',#9888,0.18,0.785398163397448);
#38=ORIENTED_CLOSED_SHELL('',*,#8896,.F.);
#43=BREP_WITH_VOIDS('Body1',#8895,(#38));
#502=SHAPE_REPRESENTATION_RELATIONSHIP('SRR','None',#17142,#552);
#552=ADVANCED_BREP_SHAPE_REPRESENTATION('',(#43),#16871);
#603=STYLED_ITEM('',(#17494),#43);
#820=FACE_BOUND('',#2068,.T.);
#1016=PLANE('',#9874);
#1017=PLANE('',#9882);
#1018=PLANE('',#9890);
#1019=PLANE('',#9891);
#1020=PLANE('',#9892);
#1021=PLANE('',#9893);
#1022=PLANE('',#9894);
#1023=PLANE('',#9895);
#1024=PLANE('',#9896);
#1025=PLANE('',#9897);
#1026=PLANE('',#9898);
#1420=FACE_OUTER_BOUND('',#2063,.T.);
#1421=FACE_OUTER_BOUND('',#2064,.T.);
#1422=FACE_OUTER_BOUND('',#2065,.T.);
#1423=FACE_OUTER_BOUND('',#2066,.T.);
#1424=FACE_OUTER_BOUND('',#2067,.T.);
#1425=FACE_OUTER_BOUND('',#2069,.T.);
#1426=FACE_OUTER_BOUND('',#2070,.T.);
#1427=FACE_OUTER_BOUND('',#2071,.T.);
#1428=FACE_OUTER_BOUND('',#2072,.T.);
#1429=FACE_OUTER_BOUND('',#2073,.T.);
#1430=FACE_OUTER_BOUND('',#2074,.T.);
#1431=FACE_OUTER_BOUND('',#2075,.T.);
#1432=FACE_OUTER_BOUND('',#2076,.T.);
#1433=FACE_OUTER_BOUND('',#2077,.T.);
#1434=FACE_OUTER_BOUND('',#2078,.T.);
#1435=FACE_OUTER_BOUND('',#2079,.T.);
#1436=FACE_OUTER_BOUND('',#2080,.T.);
#2063=EDGE_LOOP('',(#6856));
#2064=EDGE_LOOP('',(#6857,#6858,#6859,#6860));
#2065=EDGE_LOOP('',(#6861,#6862,#6863,#6864));
#2066=EDGE_LOOP('',(#6865,#6866,#6867,#6868));
#2067=EDGE_LOOP('',(#6869));
#2068=EDGE_LOOP('',(#6870));
#2069=EDGE_LOOP('',(#6871,#6872,#6873,#6874));
#2070=EDGE_LOOP('',(#6875,#6876,#6877,#6878));
#2071=EDGE_LOOP('',(#6879,#6880,#6881,#6882));
#2072=EDGE_LOOP('',(#6883));
#2073=EDGE_LOOP('',(#6884,#6885,#6886,#6887));
#2074=EDGE_LOOP('',(#6888,#6889,#6890,#6891));
#2075=EDGE_LOOP('',(#6892,#6893,#6894,#6895));
#2076=EDGE_LOOP('',(#6896,#6897,#6898,#6899));
#2077=EDGE_LOOP('',(#6900,#6901,#6902,#6903));
#2078=EDGE_LOOP('',(#6904,#6905,#6906,#6907));
#2079=EDGE_LOOP('',(#6908,#6909,#6910,#6911,#6912,#6913));
#2080=EDGE_LOOP('',(#6914,#6915,#6916,#6917,#6918,#6919));
#2709=LINE('',#14719,#3355);
#2710=LINE('',#14723,#3356);
#2711=LINE('',#14727,#3357);
#2712=LINE('',#14734,#3358);
#2713=LINE('',#14738,#3359);
#2714=LINE('',#14742,#3360);
#2715=LINE('',#14747,#3361);
#2716=LINE('',#14749,#3362);
#2717=LINE('',#14751,#3363);
#2718=LINE('',#14752,#3364);
#2719=LINE('',#14755,#3365);
#2720=LINE('',#14757,#3366);
#2721=LINE('',#14758,#3367);
#2722=LINE('',#14761,#3368);
#2723=LINE('',#14763,#3369);
#2724=LINE('',#14764,#3370);
#2725=LINE('',#14767,#3371);
#2726=LINE('',#14769,#3372);
#2727=LINE('',#14770,#3373);
#2728=LINE('',#14773,#3374);
#2729=LINE('',#14775,#3375);
#2730=LINE('',#14776,#3376);
#2731=LINE('',#14778,#3377);
#2732=LINE('',#14779,#3378);
#3355=VECTOR('',#11585,0.325);
#3356=VECTOR('',#11590,0.35);
#3357=VECTOR('',#11595,0.335);
#3358=VECTOR('',#11604,0.21);
#3359=VECTOR('',#11609,0.2);
#3360=VECTOR('',#11614,0.18);
#3361=VECTOR('',#11619,1.);
#3362=VECTOR('',#11620,1.);
#3363=VECTOR('',#11621,1.);
#3364=VECTOR('',#11622,1.);
#3365=VECTOR('',#11625,1.);
#3366=VECTOR('',#11626,1.);
#3367=VECTOR('',#11627,1.);
#3368=VECTOR('',#11630,1.);
#3369=VECTOR('',#11631,1.);
#3370=VECTOR('',#11632,1.);
#3371=VECTOR('',#11635,1.);
#3372=VECTOR('',#11636,1.);
#3373=VECTOR('',#11637,1.);
#3374=VECTOR('',#11640,1.);
#3375=VECTOR('',#11641,1.);
#3376=VECTOR('',#11642,1.);
#3377=VECTOR('',#11645,1.);
#3378=VECTOR('',#11646,1.);
#3909=CIRCLE('',#9875,0.3);
#3910=CIRCLE('',#9877,0.35);
#3911=CIRCLE('',#9879,0.35);
#3912=CIRCLE('',#9881,0.32);
#3913=CIRCLE('',#9883,0.22);
#3914=CIRCLE('',#9885,0.1954);
#3915=CIRCLE('',#9887,0.1954);
#3916=CIRCLE('',#9889,0.16);
#4445=VERTEX_POINT('',#14714);
#4446=VERTEX_POINT('',#14717);
#4447=VERTEX_POINT('',#14721);
#4448=VERTEX_POINT('',#14725);
#4449=VERTEX_POINT('',#14729);
#4450=VERTEX_POINT('',#14732);
#4451=VERTEX_POINT('',#14736);
#4452=VERTEX_POINT('',#14740);
#4453=VERTEX_POINT('',#14745);
#4454=VERTEX_POINT('',#14746);
#4455=VERTEX_POINT('',#14748);
#4456=VERTEX_POINT('',#14750);
#4457=VERTEX_POINT('',#14754);
#4458=VERTEX_POINT('',#14756);
#4459=VERTEX_POINT('',#14760);
#4460=VERTEX_POINT('',#14762);
#4461=VERTEX_POINT('',#14766);
#4462=VERTEX_POINT('',#14768);
#4463=VERTEX_POINT('',#14772);
#4464=VERTEX_POINT('',#14774);
#5326=EDGE_CURVE('',#4445,#4445,#3909,.T.);
#5327=EDGE_CURVE('',#4446,#4446,#3910,.T.);
#5328=EDGE_CURVE('',#4446,#4445,#2709,.T.);
#5329=EDGE_CURVE('',#4447,#4447,#3911,.T.);
#5330=EDGE_CURVE('',#4447,#4446,#2710,.T.);
#5331=EDGE_CURVE('',#4448,#4448,#3912,.T.);
#5332=EDGE_CURVE('',#4448,#4447,#2711,.T.);
#5333=EDGE_CURVE('',#4449,#4449,#3913,.T.);
#5334=EDGE_CURVE('',#4450,#4450,#3914,.F.);
#5335=EDGE_CURVE('',#4450,#4449,#2712,.T.);
#5336=EDGE_CURVE('',#4451,#4451,#3915,.F.);
#5337=EDGE_CURVE('',#4451,#4450,#2713,.T.);
#5338=EDGE_CURVE('',#4452,#4452,#3916,.T.);
#5339=EDGE_CURVE('',#4452,#4451,#2714,.T.);
#5340=EDGE_CURVE('',#4453,#4454,#2715,.T.);
#5341=EDGE_CURVE('',#4454,#4455,#2716,.T.);
#5342=EDGE_CURVE('',#4455,#4456,#2717,.T.);
#5343=EDGE_CURVE('',#4453,#4456,#2718,.T.);
#5344=EDGE_CURVE('',#4454,#4457,#2719,.T.);
#5345=EDGE_CURVE('',#4457,#4458,#2720,.T.);
#5346=EDGE_CURVE('',#4458,#4455,#2721,.T.);
#5347=EDGE_CURVE('',#4457,#4459,#2722,.T.);
#5348=EDGE_CURVE('',#4459,#4460,#2723,.T.);
#5349=EDGE_CURVE('',#4460,#4458,#2724,.T.);
#5350=EDGE_CURVE('',#4459,#4461,#2725,.T.);
#5351=EDGE_CURVE('',#4461,#4462,#2726,.T.);
#5352=EDGE_CURVE('',#4462,#4460,#2727,.T.);
#5353=EDGE_CURVE('',#4461,#4463,#2728,.T.);
#5354=EDGE_CURVE('',#4463,#4464,#2729,.T.);
#5355=EDGE_CURVE('',#4464,#4462,#2730,.T.);
#5356=EDGE_CURVE('',#4463,#4453,#2731,.T.);
#5357=EDGE_CURVE('',#4456,#4464,#2732,.T.);
#6856=ORIENTED_EDGE('',*,*,#5326,.F.);
#6857=ORIENTED_EDGE('',*,*,#5327,.F.);
#6858=ORIENTED_EDGE('',*,*,#5328,.T.);
#6859=ORIENTED_EDGE('',*,*,#5326,.T.);
#6860=ORIENTED_EDGE('',*,*,#5328,.F.);
#6861=ORIENTED_EDGE('',*,*,#5329,.F.);
#6862=ORIENTED_EDGE('',*,*,#5330,.T.);
#6863=ORIENTED_EDGE('',*,*,#5327,.T.);
#6864=ORIENTED_EDGE('',*,*,#5330,.F.);
#6865=ORIENTED_EDGE('',*,*,#5331,.F.);
#6866=ORIENTED_EDGE('',*,*,#5332,.T.);
#6867=ORIENTED_EDGE('',*,*,#5329,.T.);
#6868=ORIENTED_EDGE('',*,*,#5332,.F.);
#6869=ORIENTED_EDGE('',*,*,#5331,.T.);
#6870=ORIENTED_EDGE('',*,*,#5333,.F.);
#6871=ORIENTED_EDGE('',*,*,#5334,.F.);
#6872=ORIENTED_EDGE('',*,*,#5335,.T.);
#6873=ORIENTED_EDGE('',*,*,#5333,.T.);
#6874=ORIENTED_EDGE('',*,*,#5335,.F.);
#6875=ORIENTED_EDGE('',*,*,#5336,.F.);
#6876=ORIENTED_EDGE('',*,*,#5337,.T.);
#6877=ORIENTED_EDGE('',*,*,#5334,.T.);
#6878=ORIENTED_EDGE('',*,*,#5337,.F.);
#6879=ORIENTED_EDGE('',*,*,#5338,.F.);
#6880=ORIENTED_EDGE('',*,*,#5339,.T.);
#6881=ORIENTED_EDGE('',*,*,#5336,.T.);
#6882=ORIENTED_EDGE('',*,*,#5339,.F.);
#6883=ORIENTED_EDGE('',*,*,#5338,.T.);
#6884=ORIENTED_EDGE('',*,*,#5340,.T.);
#6885=ORIENTED_EDGE('',*,*,#5341,.T.);
#6886=ORIENTED_EDGE('',*,*,#5342,.T.);
#6887=ORIENTED_EDGE('',*,*,#5343,.F.);
#6888=ORIENTED_EDGE('',*,*,#5344,.T.);
#6889=ORIENTED_EDGE('',*,*,#5345,.T.);
#6890=ORIENTED_EDGE('',*,*,#5346,.T.);
#6891=ORIENTED_EDGE('',*,*,#5341,.F.);
#6892=ORIENTED_EDGE('',*,*,#5347,.T.);
#6893=ORIENTED_EDGE('',*,*,#5348,.T.);
#6894=ORIENTED_EDGE('',*,*,#5349,.T.);
#6895=ORIENTED_EDGE('',*,*,#5345,.F.);
#6896=ORIENTED_EDGE('',*,*,#5350,.T.);
#6897=ORIENTED_EDGE('',*,*,#5351,.T.);
#6898=ORIENTED_EDGE('',*,*,#5352,.T.);
#6899=ORIENTED_EDGE('',*,*,#5348,.F.);
#6900=ORIENTED_EDGE('',*,*,#5353,.T.);
#6901=ORIENTED_EDGE('',*,*,#5354,.T.);
#6902=ORIENTED_EDGE('',*,*,#5355,.T.);
#6903=ORIENTED_EDGE('',*,*,#5351,.F.);
#6904=ORIENTED_EDGE('',*,*,#5356,.T.);
#6905=ORIENTED_EDGE('',*,*,#5343,.T.);
#6906=ORIENTED_EDGE('',*,*,#5357,.T.);
#6907=ORIENTED_EDGE('',*,*,#5354,.F.);
#6908=ORIENTED_EDGE('',*,*,#5356,.F.);
#6909=ORIENTED_EDGE('',*,*,#5353,.F.);
#6910=ORIENTED_EDGE('',*,*,#5350,.F.);
#6911=ORIENTED_EDGE('',*,*,#5347,.F.);
#6912=ORIENTED_EDGE('',*,*,#5344,.F.);
#6913=ORIENTED_EDGE('',*,*,#5340,.F.);
#6914=ORIENTED_EDGE('',*,*,#5357,.F.);
#6915=ORIENTED_EDGE('',*,*,#5342,.F.);
#6916=ORIENTED_EDGE('',*,*,#5346,.F.);
#6917=ORIENTED_EDGE('',*,*,#5349,.F.);
#6918=ORIENTED_EDGE('',*,*,#5352,.F.);
#6919=ORIENTED_EDGE('',*,*,#5355,.F.);
#8275=CYLINDRICAL_SURFACE('',#9878,0.35);
#8276=CYLINDRICAL_SURFACE('',#9886,0.1954);
#8558=ADVANCED_FACE('',(#1420),#1016,.T.);
#8559=ADVANCED_FACE('',(#1421),#16,.T.);
#8560=ADVANCED_FACE('',(#1422),#8275,.T.);
#8561=ADVANCED_FACE('',(#1423),#17,.T.);
#8562=ADVANCED_FACE('',(#1424,#820),#1017,.T.);
#8563=ADVANCED_FACE('',(#1425),#18,.T.);
#8564=ADVANCED_FACE('',(#1426),#8276,.T.);
#8565=ADVANCED_FACE('',(#1427),#19,.T.);
#8566=ADVANCED_FACE('',(#1428),#1018,.T.);
#8567=ADVANCED_FACE('',(#1429),#1019,.F.);
#8568=ADVANCED_FACE('',(#1430),#1020,.F.);
#8569=ADVANCED_FACE('',(#1431),#1021,.F.);
#8570=ADVANCED_FACE('',(#1432),#1022,.F.);
#8571=ADVANCED_FACE('',(#1433),#1023,.F.);
#8572=ADVANCED_FACE('',(#1434),#1024,.F.);
#8573=ADVANCED_FACE('',(#1435),#1025,.F.);
#8574=ADVANCED_FACE('',(#1436),#1026,.F.);
#8895=CLOSED_SHELL('',(#8558,#8559,#8560,#8561,#8562,#8563,#8564,#8565,
#8566));
#8896=CLOSED_SHELL('',(#8567,#8568,#8569,#8570,#8571,#8572,#8573,#8574));
#9873=AXIS2_PLACEMENT_3D('',#14712,#11575,#11576);
#9874=AXIS2_PLACEMENT_3D('',#14713,#11577,#11578);
#9875=AXIS2_PLACEMENT_3D('',#14715,#11579,#11580);
#9876=AXIS2_PLACEMENT_3D('',#14716,#11581,#11582);
#9877=AXIS2_PLACEMENT_3D('',#14718,#11583,#11584);
#9878=AXIS2_PLACEMENT_3D('',#14720,#11586,#11587);
#9879=AXIS2_PLACEMENT_3D('',#14722,#11588,#11589);
#9880=AXIS2_PLACEMENT_3D('',#14724,#11591,#11592);
#9881=AXIS2_PLACEMENT_3D('',#14726,#11593,#11594);
#9882=AXIS2_PLACEMENT_3D('',#14728,#11596,#11597);
#9883=AXIS2_PLACEMENT_3D('',#14730,#11598,#11599);
#9884=AXIS2_PLACEMENT_3D('',#14731,#11600,#11601);
#9885=AXIS2_PLACEMENT_3D('',#14733,#11602,#11603);
#9886=AXIS2_PLACEMENT_3D('',#14735,#11605,#11606);
#9887=AXIS2_PLACEMENT_3D('',#14737,#11607,#11608);
#9888=AXIS2_PLACEMENT_3D('',#14739,#11610,#11611);
#9889=AXIS2_PLACEMENT_3D('',#14741,#11612,#11613);
#9890=AXIS2_PLACEMENT_3D('',#14743,#11615,#11616);
#9891=AXIS2_PLACEMENT_3D('',#14744,#11617,#11618);
#9892=AXIS2_PLACEMENT_3D('',#14753,#11623,#11624);
#9893=AXIS2_PLACEMENT_3D('',#14759,#11628,#11629);
#9894=AXIS2_PLACEMENT_3D('',#14765,#11633,#11634);
#9895=AXIS2_PLACEMENT_3D('',#14771,#11638,#11639);
#9896=AXIS2_PLACEMENT_3D('',#14777,#11643,#11644);
#9897=AXIS2_PLACEMENT_3D('',#14780,#11647,#11648);
#9898=AXIS2_PLACEMENT_3D('',#14781,#11649,#11650);
#11575=DIRECTION('axis',(0.,0.,1.));
#11576=DIRECTION('refdir',(1.,0.,0.));
#11577=DIRECTION('center_axis',(0.,1.,0.));
#11578=DIRECTION('ref_axis',(0.,0.,1.));
#11579=DIRECTION('center_axis',(0.,-1.,0.));
#11580=DIRECTION('ref_axis',(1.,0.,0.));
#11581=DIRECTION('center_axis',(0.,-1.,0.));
#11582=DIRECTION('ref_axis',(1.,0.,0.));
#11583=DIRECTION('center_axis',(0.,-1.,0.));
#11584=DIRECTION('ref_axis',(1.,0.,0.));
#11585=DIRECTION('',(0.707106781186547,0.707106781186548,8.65956056235493E-17));
#11586=DIRECTION('center_axis',(0.,-1.,0.));
#11587=DIRECTION('ref_axis',(1.,0.,0.));
#11588=DIRECTION('center_axis',(0.,-1.,0.));
#11589=DIRECTION('ref_axis',(1.,0.,0.));
#11590=DIRECTION('',(0.,1.,0.));
#11591=DIRECTION('center_axis',(0.,1.,0.));
#11592=DIRECTION('ref_axis',(1.,0.,0.));
#11593=DIRECTION('center_axis',(0.,-1.,0.));
#11594=DIRECTION('ref_axis',(1.,0.,0.));
#11595=DIRECTION('',(-0.707106781186547,0.707106781186548,-8.65956056235493E-17));
#11596=DIRECTION('center_axis',(0.,-1.,0.));
#11597=DIRECTION('ref_axis',(0.,0.,-1.));
#11598=DIRECTION('center_axis',(0.,-1.,0.));
#11599=DIRECTION('ref_axis',(1.,0.,0.));
#11600=DIRECTION('center_axis',(0.,1.,0.));
#11601=DIRECTION('ref_axis',(1.,0.,0.));
#11602=DIRECTION('center_axis',(0.,1.,0.));
#11603=DIRECTION('ref_axis',(1.,0.,0.));
#11604=DIRECTION('',(-0.447213595499958,0.894427190999916,-5.47678698264203E-17));
#11605=DIRECTION('center_axis',(0.,-1.,0.));
#11606=DIRECTION('ref_axis',(1.,0.,0.));
#11607=DIRECTION('center_axis',(0.,1.,0.));
#11608=DIRECTION('ref_axis',(1.,0.,0.));
#11609=DIRECTION('',(0.,1.,0.));
#11610=DIRECTION('center_axis',(0.,1.,0.));
#11611=DIRECTION('ref_axis',(1.,0.,0.));
#11612=DIRECTION('center_axis',(0.,-1.,0.));
#11613=DIRECTION('ref_axis',(1.,0.,0.));
#11614=DIRECTION('',(-0.707106781186547,0.707106781186548,-8.65956056235493E-17));
#11615=DIRECTION('center_axis',(0.,-1.,0.));
#11616=DIRECTION('ref_axis',(0.,0.,-1.));
#11617=DIRECTION('center_axis',(0.866025403784439,0.,-0.5));
#11618=DIRECTION('ref_axis',(0.5,0.,0.866025403784439));
#11619=DIRECTION('',(-0.5,0.,-0.866025403784439));
#11620=DIRECTION('',(0.,-1.,0.));
#11621=DIRECTION('',(0.5,0.,0.866025403784439));
#11622=DIRECTION('',(0.,-1.,0.));
#11623=DIRECTION('center_axis',(1.60246890531964E-16,0.,-1.));
#11624=DIRECTION('ref_axis',(1.,0.,1.60246890531964E-16));
#11625=DIRECTION('',(-1.,0.,-1.60246890531964E-16));
#11626=DIRECTION('',(0.,-1.,0.));
#11627=DIRECTION('',(1.,0.,1.60246890531964E-16));
#11628=DIRECTION('center_axis',(-0.866025403784439,0.,-0.5));
#11629=DIRECTION('ref_axis',(0.5,0.,-0.866025403784439));
#11630=DIRECTION('',(-0.5,0.,0.866025403784439));
#11631=DIRECTION('',(0.,-1.,0.));
#11632=DIRECTION('',(0.5,0.,-0.866025403784439));
#11633=DIRECTION('center_axis',(-0.866025403784439,0.,0.5));
#11634=DIRECTION('ref_axis',(-0.5,0.,-0.866025403784439));
#11635=DIRECTION('',(0.5,0.,0.866025403784439));
#11636=DIRECTION('',(0.,-1.,0.));
#11637=DIRECTION('',(-0.5,0.,-0.866025403784439));
#11638=DIRECTION('center_axis',(-1.60246890531964E-16,0.,1.));
#11639=DIRECTION('ref_axis',(-1.,0.,-1.60246890531964E-16));
#11640=DIRECTION('',(1.,0.,1.60246890531964E-16));
#11641=DIRECTION('',(0.,-1.,0.));
#11642=DIRECTION('',(-1.,0.,-1.60246890531964E-16));
#11643=DIRECTION('center_axis',(0.866025403784439,0.,0.5));
#11644=DIRECTION('ref_axis',(-0.5,0.,0.866025403784439));
#11645=DIRECTION('',(0.5,0.,-0.866025403784439));
#11646=DIRECTION('',(-0.5,0.,0.866025403784439));
#11647=DIRECTION('center_axis',(0.,1.,0.));
#11648=DIRECTION('ref_axis',(1.,0.,0.));
#11649=DIRECTION('center_axis',(0.,-1.,0.));
#11650=DIRECTION('ref_axis',(0.,0.,-1.));
#14712=CARTESIAN_POINT('',(0.,0.,0.));
#14713=CARTESIAN_POINT('Origin',(0.3,0.4,0.));
#14714=CARTESIAN_POINT('',(-0.3,0.4,-3.67394039744206E-17));
#14715=CARTESIAN_POINT('Origin',(0.,0.4,0.));
#14716=CARTESIAN_POINT('Origin',(0.,0.375,0.));
#14717=CARTESIAN_POINT('',(-0.35,0.35,-4.28626379701573E-17));
#14718=CARTESIAN_POINT('Origin',(0.,0.35,0.));
#14719=CARTESIAN_POINT('',(-0.325,0.375,-3.9801020972289E-17));
#14720=CARTESIAN_POINT('Origin',(0.,0.19,0.));
#14721=CARTESIAN_POINT('',(-0.35,0.03,-4.28626379701574E-17));
#14722=CARTESIAN_POINT('Origin',(0.,0.03,0.));
#14723=CARTESIAN_POINT('',(-0.35,0.19,-4.28626379701574E-17));
#14724=CARTESIAN_POINT('Origin',(0.,0.0149999999999999,0.));
#14725=CARTESIAN_POINT('',(-0.32,-3.29597460435593E-17,-3.91886975727153E-17));
#14726=CARTESIAN_POINT('Origin',(0.,0.,0.));
#14727=CARTESIAN_POINT('',(-0.335,0.0149999999999999,-4.10256677714363E-17));
#14728=CARTESIAN_POINT('Origin',(0.22,0.,0.));
#14729=CARTESIAN_POINT('',(-0.22,-6.93889390390723E-18,-2.69422295812418E-17));
#14730=CARTESIAN_POINT('Origin',(0.,0.,0.));
#14731=CARTESIAN_POINT('Origin',(0.,-0.02,0.));
#14732=CARTESIAN_POINT('',(-0.1954,-0.0492,2.39295984553393E-17));
#14733=CARTESIAN_POINT('Origin',(0.,-0.0492,0.));
#14734=CARTESIAN_POINT('',(-0.21,-0.02,-2.57175827820944E-17));
#14735=CARTESIAN_POINT('Origin',(0.,-0.8,0.));
#14736=CARTESIAN_POINT('',(-0.1954,-1.5646,2.39295984553393E-17));
#14737=CARTESIAN_POINT('Origin',(0.,-1.5646,0.));
#14738=CARTESIAN_POINT('',(-0.1954,-0.8,-2.39295984553393E-17));
#14739=CARTESIAN_POINT('Origin',(0.,-1.58,0.));
#14740=CARTESIAN_POINT('',(-0.16,-1.6,-1.95943487863577E-17));
#14741=CARTESIAN_POINT('Origin',(0.,-1.6,0.));
#14742=CARTESIAN_POINT('',(-0.18,-1.58,-2.20436423846524E-17));
#14743=CARTESIAN_POINT('Origin',(0.,-1.6,0.));
#14744=CARTESIAN_POINT('Origin',(0.0866025403784439,-0.4,-0.15));
#14745=CARTESIAN_POINT('',(0.173205080756888,-0.4,0.));
#14746=CARTESIAN_POINT('',(0.0866025403784439,-0.4,-0.15));
#14747=CARTESIAN_POINT('',(0.173205080756888,-0.4,0.));
#14748=CARTESIAN_POINT('',(0.0866025403784439,-0.64,-0.15));
#14749=CARTESIAN_POINT('',(0.0866025403784439,-0.4,-0.15));
#14750=CARTESIAN_POINT('',(0.173205080756888,-0.64,0.));
#14751=CARTESIAN_POINT('',(0.173205080756888,-0.64,0.));
#14752=CARTESIAN_POINT('',(0.173205080756888,-0.4,0.));
#14753=CARTESIAN_POINT('Origin',(-0.0866025403784438,-0.4,-0.15));
#14754=CARTESIAN_POINT('',(-0.0866025403784438,-0.4,-0.15));
#14755=CARTESIAN_POINT('',(0.0866025403784439,-0.4,-0.15));
#14756=CARTESIAN_POINT('',(-0.0866025403784438,-0.64,-0.15));
#14757=CARTESIAN_POINT('',(-0.0866025403784438,-0.4,-0.15));
#14758=CARTESIAN_POINT('',(0.0866025403784439,-0.64,-0.15));
#14759=CARTESIAN_POINT('Origin',(-0.173205080756888,-0.4,-2.77555756156289E-17));
#14760=CARTESIAN_POINT('',(-0.173205080756888,-0.4,-2.12115047744981E-17));
#14761=CARTESIAN_POINT('',(-0.0866025403784438,-0.4,-0.15));
#14762=CARTESIAN_POINT('',(-0.173205080756888,-0.64,-2.77555756156289E-17));
#14763=CARTESIAN_POINT('',(-0.173205080756888,-0.4,-2.12115047744981E-17));
#14764=CARTESIAN_POINT('',(-0.0866025403784438,-0.64,-0.15));
#14765=CARTESIAN_POINT('Origin',(-0.0866025403784439,-0.4,0.15));
#14766=CARTESIAN_POINT('',(-0.0866025403784439,-0.4,0.15));
#14767=CARTESIAN_POINT('',(-0.173205080756888,-0.4,-2.12115047744981E-17));
#14768=CARTESIAN_POINT('',(-0.0866025403784439,-0.64,0.15));
#14769=CARTESIAN_POINT('',(-0.0866025403784439,-0.4,0.15));
#14770=CARTESIAN_POINT('',(-0.173205080756888,-0.64,-2.12115047744981E-17));
#14771=CARTESIAN_POINT('Origin',(0.0866025403784439,-0.4,0.15));
#14772=CARTESIAN_POINT('',(0.0866025403784439,-0.4,0.15));
#14773=CARTESIAN_POINT('',(-0.0866025403784439,-0.4,0.15));
#14774=CARTESIAN_POINT('',(0.0866025403784439,-0.64,0.15));
#14775=CARTESIAN_POINT('',(0.0866025403784439,-0.4,0.15));
#14776=CARTESIAN_POINT('',(-0.0866025403784439,-0.64,0.15));
#14777=CARTESIAN_POINT('Origin',(0.173205080756888,-0.4,0.));
#14778=CARTESIAN_POINT('',(0.0866025403784439,-0.4,0.15));
#14779=CARTESIAN_POINT('',(0.0866025403784439,-0.64,0.15));
#14780=CARTESIAN_POINT('Origin',(0.,-0.4,-2.77555756156289E-17));
#14781=CARTESIAN_POINT('Origin',(0.,-0.64,-2.77555756156289E-17));
#16812=UNCERTAINTY_MEASURE_WITH_UNIT(LENGTH_MEASURE(0.001),#16912,
'DISTANCE_ACCURACY_VALUE',
'Maximum model space distance between geometric entities at asserted c
onnectivities');
#16852=UNCERTAINTY_MEASURE_WITH_UNIT(LENGTH_MEASURE(0.001),#16912,
'DISTANCE_ACCURACY_VALUE',
'Maximum model space distance between geometric entities at asserted c
onnectivities');
#16871=(
GEOMETRIC_REPRESENTATION_CONTEXT(3)
GLOBAL_UNCERTAINTY_ASSIGNED_CONTEXT((#16812))
GLOBAL_UNIT_ASSIGNED_CONTEXT((#16912,#16914,#16915))
REPRESENTATION_CONTEXT('','3D')
);
#16911=(
GEOMETRIC_REPRESENTATION_CONTEXT(3)
GLOBAL_UNCERTAINTY_ASSIGNED_CONTEXT((#16852))
GLOBAL_UNIT_ASSIGNED_CONTEXT((#16912,#16914,#16915))
REPRESENTATION_CONTEXT('','3D')
);
#16912=(
LENGTH_UNIT()
NAMED_UNIT(*)
SI_UNIT(.CENTI.,.METRE.)
);
#16914=(
NAMED_UNIT(*)
PLANE_ANGLE_UNIT()
SI_UNIT($,.RADIAN.)
);
#16915=(
NAMED_UNIT(*)
SI_UNIT($,.STERADIAN.)
SOLID_ANGLE_UNIT()
);
#16934=SHAPE_DEFINITION_REPRESENTATION(#16994,#17142);
#16994=PRODUCT_DEFINITION_SHAPE('',$,#17201);
#17142=SHAPE_REPRESENTATION('',(#9873),#16871);
#17182=PRODUCT_DEFINITION_CONTEXT('part definition',#17358,'design');
#17201=PRODUCT_DEFINITION('Cap Screw - M4x16','Cap Screw - M4x16',#17259,
#17182);
#17259=PRODUCT_DEFINITION_FORMATION('',$,#17378);
#17358=APPLICATION_CONTEXT(
'Core Data for Automotive Mechanical Design Process');
#17359=PRODUCT_CONTEXT('part definition',#17358,'mechanical');
#17378=PRODUCT('Cap Screw - M4x16','Cap Screw - M4x16',
'Cap Screw - M4x16',(#17359));
#17488=COLOUR_RGB('Black',0.12,0.14,0.17);
#17489=FILL_AREA_STYLE_COLOUR('',#17488);
#17490=FILL_AREA_STYLE('',(#17489));
#17491=SURFACE_STYLE_FILL_AREA(#17490);
#17492=SURFACE_SIDE_STYLE('',(#17491));
#17493=SURFACE_STYLE_USAGE(.BOTH.,#17492);
#17494=PRESENTATION_STYLE_ASSIGNMENT((#17493));
ENDSEC;
END-ISO-10303-21;
